ISO-10303-21;
HEADER;
FILE_DESCRIPTION (('STEP AP214'),
    '1' );
FILE_NAME ('socket button head screw_iso_ISO 7380 - M5 x 25 - 25N.step',
    '2026-10-05T20:22:16',
    ( '' ),
    ( '' ),
    'SwSTEP 2.0',
    'SolidWorks 2026',
    '' );
FILE_SCHEMA (( 'AUTOMOTIVE_DESIGN' ));
ENDSEC;

DATA;
#16=ORIENTED_EDGE ( 'NONE', *, *, #13429, .F. ) ;
#36=DIRECTION ( 'NONE',  ( -1.000000000000000000, 0.000000000000000000, 0.000000000000000000 ) ) ;
#40=AXIS2_PLACEMENT_3D ( 'NONE', #14825, #13678, #6691 ) ;
#41=ORIENTED_EDGE ( 'NONE', *, *, #303, .F. ) ;
#71=DIRECTION ( 'NONE',  ( -1.000000000000000000, 0.000000000000000000, 0.000000000000000000 ) ) ;
#77=EDGE_CURVE ( 'NONE', #13658, #4758, #14864, .T. ) ;
#86=APPLICATION_CONTEXT ( 'automotive_design' ) ;
#92=CARTESIAN_POINT ( 'NONE',  ( 2.370000000000000551, 0.000000000000000000, 0.000000000000000000 ) ) ;
#118=VERTEX_POINT ( 'NONE', #16766 ) ;
#121=AXIS2_PLACEMENT_3D ( 'NONE', #12390, #5748, #16650 ) ;
#151=CARTESIAN_POINT ( 'NONE',  ( 1.559999999999998943, 1.732050807568885631, 0.000000000000000000 ) ) ;
#188=AXIS2_PLACEMENT_3D ( 'NONE', #16749, #13998, #10087 ) ;
#198=VECTOR ( 'NONE', #10876, 1000.000000000000000 ) ;
#245=ADVANCED_FACE ( 'NONE', ( #10458, #10362 ), #15773, .T. ) ;
#297=DIRECTION ( 'NONE',  ( 0.000000000000000000, 0.000000000000000000, 1.000000000000000000 ) ) ;
#303=EDGE_CURVE ( 'NONE', #12797, #10037, #6701, .T. ) ;
#304=FACE_OUTER_BOUND ( 'NONE', #8211, .T. ) ;
#307=ORIENTED_EDGE ( 'NONE', *, *, #3862, .T. ) ;
#336=ADVANCED_FACE ( 'NONE', ( #9394 ), #7794, .F. ) ;
#349=CARTESIAN_POINT ( 'NONE',  ( 0.000000000000000000, 3.061616997868382155E-16, -2.499999999999999112 ) ) ;
#353=ORIENTED_EDGE ( 'NONE', *, *, #661, .F. ) ;
#374=VERTEX_POINT ( 'NONE', #16306 ) ;
#378=ORIENTED_EDGE ( 'NONE', *, *, #1221, .T. ) ;
#388=DIRECTION ( 'NONE',  ( 0.000000000000000000, -0.4999999999999997224, 0.8660254037844387076 ) ) ;
#403=EDGE_LOOP ( 'NONE', ( #5681, #2940, #16094, #11500 ) ) ;
#440=DIRECTION ( 'NONE',  ( -1.000000000000000000, 0.000000000000000000, 0.000000000000000000 ) ) ;
#442=ORIENTED_EDGE ( 'NONE', *, *, #11491, .T. ) ;
#472=VECTOR ( 'NONE', #10118, 1000.000000000000114 ) ;
#482=CARTESIAN_POINT ( 'NONE',  ( 2.370000000000000551, -4.750000000000000888, -5.817072295949928412E-16 ) ) ;
#550=DIRECTION ( 'NONE',  ( 0.000000000000000000, 0.000000000000000000, 1.000000000000000000 ) ) ;
#598=DIRECTION ( 'NONE',  ( 0.000000000000000000, 1.000000000000000000, 0.000000000000000000 ) ) ;
#645=CARTESIAN_POINT ( 'NONE',  ( 27.75000000000000000, 0.000000000000000000, 0.000000000000000000 ) ) ;
#659=CARTESIAN_POINT ( 'NONE',  ( 1.559999999999998943, 1.299038105676664223, 0.7500000000000006661 ) ) ;
#661=EDGE_CURVE ( 'NONE', #8817, #10086, #2457, .T. ) ;
#678=CARTESIAN_POINT ( 'NONE',  ( 0.000000000000000000, -2.375000000000000000, -4.362804221962446556E-16 ) ) ;
#694=CIRCLE ( 'NONE', #3507, 4.750000000000000000 ) ;
#759=AXIS2_PLACEMENT_3D ( 'NONE', #15935, #15665, #6285 ) ;
#762=ADVANCED_FACE ( 'NONE', ( #2735, #8126 ), #14943, .F. ) ;
#818=VECTOR ( 'NONE', #1736, 1000.000000000000000 ) ;
#831=DIRECTION ( 'NONE',  ( -1.000000000000000000, 0.000000000000000000, 0.000000000000000000 ) ) ;
#868=DIRECTION ( 'NONE',  ( -1.000000000000000000, 0.000000000000000000, 0.000000000000000000 ) ) ;
#891=ORIENTED_EDGE ( 'NONE', *, *, #2427, .F. ) ;
#903=VERTEX_POINT ( 'NONE', #3255 ) ;
#915=CARTESIAN_POINT ( 'NONE',  ( 2.950000000000001066, 0.000000000000000000, 2.499999999999999112 ) ) ;
#1005=EDGE_LOOP ( 'NONE', ( #12594, #1908, #10659, #13298, #353 ) ) ;
#1049=ORIENTED_EDGE ( 'NONE', *, *, #6936, .F. ) ;
#1062=CARTESIAN_POINT ( 'NONE',  ( 0.000000000000000000, 0.000000000000000000, 0.000000000000000000 ) ) ;
#1068=AXIS2_PLACEMENT_3D ( 'NONE', #3841, #36, #5435 ) ;
#1122=AXIS2_PLACEMENT_3D ( 'NONE', #1780, #8415, #7174 ) ;
#1169=CARTESIAN_POINT ( 'NONE',  ( 1.559999999999998943, -1.732050807568885631, 0.000000000000000000 ) ) ;
#1211=EDGE_LOOP ( 'NONE', ( #16, #8549, #7703 ) ) ;
#1219=VERTEX_POINT ( 'NONE', #8634 ) ;
#1221=EDGE_CURVE ( 'NONE', #10037, #12789, #8487, .T. ) ;
#1229=ORIENTED_EDGE ( 'NONE', *, *, #5759, .T. ) ;
#1255=EDGE_CURVE ( 'NONE', #4882, #15354, #16487, .T. ) ;
#1261=DIRECTION ( 'NONE',  ( -1.000000000000000000, 0.000000000000000000, 0.000000000000000000 ) ) ;
#1308=DIRECTION ( 'NONE',  ( 0.000000000000000000, 0.000000000000000000, 1.000000000000000000 ) ) ;
#1319=ORIENTED_EDGE ( 'NONE', *, *, #6992, .F. ) ;
#1384=EDGE_CURVE ( 'NONE', #12997, #2044, #3662, .T. ) ;
#1396=AXIS2_PLACEMENT_3D ( 'NONE', #9053, #831, #17027 ) ;
#1417=CONICAL_SURFACE ( 'NONE', #5376, 1732.050807568857181, 1.047197551196592746 ) ;
#1440=DIRECTION ( 'NONE',  ( 1.000000000000000000, 0.000000000000000000, 0.000000000000000000 ) ) ;
#1450=CARTESIAN_POINT ( 'NONE',  ( 27.75000000000000000, 0.000000000000000000, 0.000000000000000000 ) ) ;
#1522=CARTESIAN_POINT ( 'NONE',  ( 2.370000000000000551, 5.817072295949927426E-16, -4.750000000000000000 ) ) ;
#1552=CARTESIAN_POINT ( 'NONE',  ( 0.000000000000000000, 1.732050807568885631, 0.000000000000000000 ) ) ;
#1586=VECTOR ( 'NONE', #4728, 1000.000000000000000 ) ;
#1588=CIRCLE ( 'NONE', #16861, 1.500000000000000000 ) ;
#1607=FACE_OUTER_BOUND ( 'NONE', #1211, .T. ) ;
#1614=AXIS2_PLACEMENT_3D ( 'NONE', #4696, #8584, #7260 ) ;
#1625=PLANE ( 'NONE',  #5932 ) ;
#1627=ORIENTED_EDGE ( 'NONE', *, *, #7314, .F. ) ;
#1652=VERTEX_POINT ( 'NONE', #12212 ) ;
#1668=PLANE ( 'NONE',  #16897 ) ;
#1716=FACE_OUTER_BOUND ( 'NONE', #8856, .T. ) ;
#1731=CARTESIAN_POINT ( 'NONE',  ( 0.000000000000000000, 0.8660254037844428154, 1.500000000000001332 ) ) ;
#1735=CARTESIAN_POINT ( 'NONE',  ( 1.559999999999998943, -1.732050807568885631, 0.000000000000000000 ) ) ;
#1736=DIRECTION ( 'NONE',  ( 0.000000000000000000, -1.000000000000000000, 0.000000000000000000 ) ) ;
#1780=CARTESIAN_POINT ( 'NONE',  ( 2.749999999999999112, 0.000000000000000000, 0.000000000000000000 ) ) ;
#1788=DIRECTION ( 'NONE',  ( -1.000000000000000000, 0.000000000000000000, 0.000000000000000000 ) ) ;
#1801=CARTESIAN_POINT ( 'NONE',  ( 1.559999999999998943, 0.8660254037844428154, -1.499999999999997780 ) ) ;
#1806=FACE_OUTER_BOUND ( 'NONE', #8014, .T. ) ;
#1811=DIRECTION ( 'NONE',  ( 0.000000000000000000, 0.4999999999999996669, 0.8660254037844388186 ) ) ;
#1832=CARTESIAN_POINT ( 'NONE',  ( 0.000000000000000000, 0.000000000000000000, 0.000000000000000000 ) ) ;
#1862=EDGE_CURVE ( 'NONE', #6587, #8018, #8542, .T. ) ;
#1908=ORIENTED_EDGE ( 'NONE', *, *, #7738, .T. ) ;
#1943=AXIS2_PLACEMENT_3D ( 'NONE', #8786, #12852, #6124 ) ;
#1944=DIRECTION ( 'NONE',  ( -1.000000000000000000, 0.000000000000000000, 0.000000000000000000 ) ) ;
#1957=CARTESIAN_POINT ( 'NONE',  ( 1.559999999999998943, 0.8660254037844428154, 1.500000000000001332 ) ) ;
#1972=LINE ( 'NONE', #9934, #8169 ) ;
#1982=ORIENTED_EDGE ( 'NONE', *, *, #16978, .F. ) ;
#2001=ORIENTED_EDGE ( 'NONE', *, *, #16740, .T. ) ;
#2030=ORIENTED_EDGE ( 'NONE', *, *, #3884, .T. ) ;
#2044=VERTEX_POINT ( 'NONE', #13857 ) ;
#2055=EDGE_CURVE ( 'NONE', #8718, #8018, #5970, .T. ) ;
#2056=CARTESIAN_POINT ( 'NONE',  ( 1.559999999999998943, -1.732050807568885631, 0.000000000000000000 ) ) ;
#2088=FACE_OUTER_BOUND ( 'NONE', #403, .T. ) ;
#2126=CARTESIAN_POINT ( 'NONE',  ( 1.559999999999998943, 0.8660254037844428154, 1.500000000000001332 ) ) ;
#2129=ADVANCED_FACE ( 'NONE', ( #304 ), #7196, .T. ) ;
#2141=VERTEX_POINT ( 'NONE', #1801 ) ;
#2161=AXIS2_PLACEMENT_3D ( 'NONE', #1169, #9304, #17459 ) ;
#2162=AXIS2_PLACEMENT_3D ( 'NONE', #11423, #7100, #7179 ) ;
#2185=PRESENTATION_STYLE_ASSIGNMENT (( #9357 ) ) ;
#2312=ORIENTED_EDGE ( 'NONE', *, *, #10648, .F. ) ;
#2328=CARTESIAN_POINT ( 'NONE',  ( 1.559999999999998943, -1.299038105676664223, -0.7500000000000006661 ) ) ;
#2398=EDGE_CURVE ( 'NONE', #8931, #12797, #14184, .T. ) ;
#2420=ORIENTED_EDGE ( 'NONE', *, *, #4150, .T. ) ;
#2427=EDGE_CURVE ( 'NONE', #12997, #13658, #4816, .T. ) ;
#2442=CARTESIAN_POINT ( 'NONE',  ( 2.426025403784448642, 0.000000000000000000, 0.000000000000000000 ) ) ;
#2449=FILL_AREA_STYLE ('',( #6435 ) ) ;
#2457=CIRCLE ( 'NONE', #1614, 5.315148208181398104 ) ;
#2463=COLOUR_RGB ( '', 0.72549020, 0.75294118, 0.79215686) ;
#2562=DIRECTION ( 'NONE',  ( 0.000000000000000000, 1.000000000000000000, 0.000000000000000000 ) ) ;
#2564=DIRECTION ( 'NONE',  ( -0.7071067811865513475, 0.000000000000000000, 0.7071067811865436870 ) ) ;
#2620=CYLINDRICAL_SURFACE ( 'NONE', #40, 4.750000000000000000 ) ;
#2623=VERTEX_POINT ( 'NONE', #9287 ) ;
#2647=EDGE_LOOP ( 'NONE', ( #41, #6678, #14964 ) ) ;
#2681=EDGE_CURVE ( 'NONE', #1652, #10063, #3968, .T. ) ;
#2694=ORIENTED_EDGE ( 'NONE', *, *, #13429, .T. ) ;
#2728=AXIS2_PLACEMENT_3D ( 'NONE', #6116, #15241, #6030 ) ;
#2735=FACE_BOUND ( 'NONE', #13791, .T. ) ;
#2810=SHAPE_DEFINITION_REPRESENTATION ( #12375, #6585 ) ;
#2823=CARTESIAN_POINT ( 'NONE',  ( 2.749999999999999112, 2.500000000000002220, 0.000000000000000000 ) ) ;
#2868=CARTESIAN_POINT ( 'NONE',  ( 1.559999999999998943, 0.8660254037844428154, -1.499999999999997780 ) ) ;
#2876=FACE_OUTER_BOUND ( 'NONE', #9302, .T. ) ;
#2940=ORIENTED_EDGE ( 'NONE', *, *, #6959, .T. ) ;
#2952=ORIENTED_EDGE ( 'NONE', *, *, #7429, .F. ) ;
#2972=( NAMED_UNIT ( * ) PLANE_ANGLE_UNIT ( ) SI_UNIT ( $, .RADIAN. ) );
#2984=CARTESIAN_POINT ( 'NONE',  ( 1.559999999999998943, -0.8660254037844428154, -1.499999999999997780 ) ) ;
#3005=DIRECTION ( 'NONE',  ( 0.000000000000000000, 0.000000000000000000, 1.000000000000000000 ) ) ;
#3015=AXIS2_PLACEMENT_3D ( 'NONE', #17080, #10522, #5040 ) ;
#3037=AXIS2_PLACEMENT_3D ( 'NONE', #12372, #71, #5649 ) ;
#3071=DIRECTION ( 'NONE',  ( -1.000000000000000000, 0.000000000000000000, 0.000000000000000000 ) ) ;
#3110=ORIENTED_EDGE ( 'NONE', *, *, #4202, .F. ) ;
#3113=FACE_OUTER_BOUND ( 'NONE', #12070, .T. ) ;
#3123=ORIENTED_EDGE ( 'NONE', *, *, #4202, .T. ) ;
#3160=( LENGTH_UNIT ( ) NAMED_UNIT ( * ) SI_UNIT ( .MILLI., .METRE. ) );
#3251=DIRECTION ( 'NONE',  ( -0.5000000000000042188, 0.000000000000000000, 0.8660254037844361541 ) ) ;
#3254=CONICAL_SURFACE ( 'NONE', #13144, 2.055000000000000160, 0.7853981633974428389 ) ;
#3255=CARTESIAN_POINT ( 'NONE',  ( 27.75000000000000000, 0.000000000000000000, 2.055000000000000160 ) ) ;
#3294=CIRCLE ( 'NONE', #759, 2.699999999999999289 ) ;
#3320=ORIENTED_EDGE ( 'NONE', *, *, #4150, .F. ) ;
#3369=ORIENTED_EDGE ( 'NONE', *, *, #4116, .F. ) ;
#3376=EDGE_LOOP ( 'NONE', ( #6301, #7871, #10654, #1627, #10607 ) ) ;
#3426=SPHERICAL_SURFACE ( 'NONE', #12135, 5.315148208181398104 ) ;
#3438=DIRECTION ( 'NONE',  ( -1.000000000000000000, 0.000000000000000000, 0.000000000000000000 ) ) ;
#3500=( NAMED_UNIT ( * ) PLANE_ANGLE_UNIT ( ) SI_UNIT ( $, .RADIAN. ) );
#3507=AXIS2_PLACEMENT_3D ( 'NONE', #16272, #16001, #1308 ) ;
#3513=CARTESIAN_POINT ( 'NONE',  ( 2.426025403784448642, 0.000000000000000000, 2.168404344971008868E-16 ) ) ;
#3545=DIRECTION ( 'NONE',  ( 0.000000000000000000, 1.000000000000000000, 1.224646799147353207E-16 ) ) ;
#3556=LINE ( 'NONE', #2056, #6781 ) ;
#3583=AXIS2_PLACEMENT_3D ( 'NONE', #5482, #6893, #8222 ) ;
#3662=CIRCLE ( 'NONE', #1122, 2.699999999999999289 ) ;
#3719=ORIENTED_EDGE ( 'NONE', *, *, #10259, .T. ) ;
#3733=ORIENTED_EDGE ( 'NONE', *, *, #5759, .F. ) ;
#3753=ADVANCED_FACE ( 'NONE', ( #5315 ), #10709, .T. ) ;
#3801=ORIENTED_EDGE ( 'NONE', *, *, #12863, .F. ) ;
#3810=CARTESIAN_POINT ( 'NONE',  ( 1.559999999999998943, -1.732050807568885631, 0.000000000000000000 ) ) ;
#3841=CARTESIAN_POINT ( 'NONE',  ( 0.000000000000000000, 0.000000000000000000, 0.000000000000000000 ) ) ;
#3843=ORIENTED_EDGE ( 'NONE', *, *, #11224, .T. ) ;
#3862=EDGE_CURVE ( 'NONE', #374, #8817, #16644, .T. ) ;
#3873=AXIS2_PLACEMENT_3D ( 'NONE', #14623, #4015, #17187 ) ;
#3875=VECTOR ( 'NONE', #11057, 1000.000000000000114 ) ;
#3884=EDGE_CURVE ( 'NONE', #13912, #15454, #12673, .T. ) ;
#3892=LINE ( 'NONE', #12119, #10030 ) ;
#3968=CIRCLE ( 'NONE', #6217, 4.750000000000000000 ) ;
#4015=DIRECTION ( 'NONE',  ( -1.000000000000000000, 0.000000000000000000, 0.000000000000000000 ) ) ;
#4019=ORIENTED_EDGE ( 'NONE', *, *, #661, .T. ) ;
#4063=CARTESIAN_POINT ( 'NONE',  ( 1.559999999999998943, 0.000000000000000000, 0.000000000000000000 ) ) ;
#4066=CARTESIAN_POINT ( 'NONE',  ( 27.75000000000000000, 2.516649172247811061E-16, -2.055000000000000160 ) ) ;
#4083=DIRECTION ( 'NONE',  ( 0.000000000000000000, 0.000000000000000000, 1.000000000000000000 ) ) ;
#4116=EDGE_CURVE ( 'NONE', #2623, #8731, #17243, .T. ) ;
#4130=AXIS2_PLACEMENT_3D ( 'NONE', #15253, #6857, #297 ) ;
#4134=ORIENTED_EDGE ( 'NONE', *, *, #7385, .F. ) ;
#4150=EDGE_CURVE ( 'NONE', #8931, #8731, #15999, .T. ) ;
#4167=DIRECTION ( 'NONE',  ( 0.000000000000000000, 0.000000000000000000, 1.000000000000000000 ) ) ;
#4183=PRODUCT ( 'socket button head screw_iso_ISO 7380 - M5 x 25 - 25N', 'socket button head screw_iso_ISO 7380 - M5 x 25 - 25N', '', ( #11830 ) ) ;
#4185=EDGE_CURVE ( 'NONE', #8740, #4376, #12395, .T. ) ;
#4202=EDGE_CURVE ( 'NONE', #118, #903, #8734, .T. ) ;
#4232=DIRECTION ( 'NONE',  ( 0.000000000000000000, 0.000000000000000000, 1.000000000000000000 ) ) ;
#4238=DIRECTION ( 'NONE',  ( -0.7071067811865513475, 8.659560562354886020E-17, -0.7071067811865436870 ) ) ;
#4254=LINE ( 'NONE', #5667, #3875 ) ;
#4263=VECTOR ( 'NONE', #10494, 1000.000000000000114 ) ;
#4340=DIRECTION ( 'NONE',  ( 0.000000000000000000, 0.4999999999999997780, -0.8660254037844387076 ) ) ;
#4345=EDGE_LOOP ( 'NONE', ( #7028, #6429, #10102 ) ) ;
#4346=PLANE ( 'NONE',  #8881 ) ;
#4364=ADVANCED_FACE ( 'NONE', ( #12726 ), #3426, .T. ) ;
#4374=DIRECTION ( 'NONE',  ( -1.000000000000000000, 0.000000000000000000, 0.000000000000000000 ) ) ;
#4376=VERTEX_POINT ( 'NONE', #678 ) ;
#4399=ORIENTED_EDGE ( 'NONE', *, *, #1255, .T. ) ;
#4423=DIRECTION ( 'NONE',  ( -1.000000000000000000, 0.000000000000000000, 0.000000000000000000 ) ) ;
#4440=ORIENTED_EDGE ( 'NONE', *, *, #7209, .T. ) ;
#4491=PRODUCT_DEFINITION ( 'UNKNOWN', '', #9255, #8364 ) ;
#4535=CARTESIAN_POINT ( 'NONE',  ( 1.559999999999998943, -1.732050807568885631, 0.000000000000000000 ) ) ;
#4596=DIRECTION ( 'NONE',  ( 0.000000000000000000, 0.000000000000000000, 1.000000000000000000 ) ) ;
#4606=CARTESIAN_POINT ( 'NONE',  ( 1.559999999999998943, 0.8660254037844428154, -1.499999999999997780 ) ) ;
#4616=ORIENTED_EDGE ( 'NONE', *, *, #2681, .F. ) ;
#4629=EDGE_LOOP ( 'NONE', ( #13160, #3123, #3843, #6326 ) ) ;
#4682=ADVANCED_FACE ( 'NONE', ( #1806 ), #5351, .F. ) ;
#4688=CARTESIAN_POINT ( 'NONE',  ( 1.559999999999998943, 1.299038105676664223, -0.7500000000000006661 ) ) ;
#4696=CARTESIAN_POINT ( 'NONE',  ( 4.755015822784812052, 0.000000000000000000, 0.000000000000000000 ) ) ;
#4728=DIRECTION ( 'NONE',  ( -1.000000000000000000, 0.000000000000000000, 0.000000000000000000 ) ) ;
#4732=DIRECTION ( 'NONE',  ( 0.000000000000000000, 0.000000000000000000, -1.000000000000000000 ) ) ;
#4758=VERTEX_POINT ( 'NONE', #915 ) ;
#4816=CIRCLE ( 'NONE', #17245, 0.2000000000000000944 ) ;
#4830=ORIENTED_EDGE ( 'NONE', *, *, #12515, .T. ) ;
#4875=ADVANCED_BREP_SHAPE_REPRESENTATION ( '', ( #16934, #3583 ), #14620 ) ;
#4882=VERTEX_POINT ( 'NONE', #9744 ) ;
#4883=DIRECTION ( 'NONE',  ( 0.000000000000000000, 0.000000000000000000, -1.000000000000000000 ) ) ;
#4890=DIRECTION ( 'NONE',  ( 0.000000000000000000, -0.5000000000000011102, 0.8660254037844380415 ) ) ;
#4906=ADVANCED_FACE ( 'NONE', ( #11253 ), #8891, .T. ) ;
#4909=SHAPE_REPRESENTATION_RELATIONSHIP ( 'NONE' , 'NONE' ,  #6585, #4875 ) ;
#4939=APPLICATION_CONTEXT ( 'automotive_design' ) ;
#4950=CARTESIAN_POINT ( 'NONE',  ( 27.30499999999999616, 0.000000000000000000, 2.499999999999999556 ) ) ;
#4969=CIRCLE ( 'NONE', #12609, 4.750000000000000000 ) ;
#4976=PLANE ( 'NONE',  #14587 ) ;
#4995=AXIS2_PLACEMENT_3D ( 'NONE', #5144, #12787, #4732 ) ;
#4999=CIRCLE ( 'NONE', #10074, 4.750000000000000000 ) ;
#5010=VECTOR ( 'NONE', #12391, 1000.000000000000000 ) ;
#5036=AXIS2_PLACEMENT_3D ( 'NONE', #10966, #15215, #16384 ) ;
#5040=DIRECTION ( 'NONE',  ( 0.000000000000000000, 0.000000000000000000, 1.000000000000000000 ) ) ;
#5057=DIRECTION ( 'NONE',  ( 0.000000000000000000, 0.000000000000000000, -1.000000000000000000 ) ) ;
#5086=UNCERTAINTY_MEASURE_WITH_UNIT (LENGTH_MEASURE( 1.000000000000000082E-05 ), #16360, 'distance_accuracy_value', 'NONE');
#5090=ADVANCED_FACE ( 'NONE', ( #6467 ), #3254, .T. ) ;
#5092=EDGE_CURVE ( 'NONE', #12797, #1219, #10447, .T. ) ;
#5118=CARTESIAN_POINT ( 'NONE',  ( 0.000000000000000000, 1.732050807568885631, 0.000000000000000000 ) ) ;
#5144=CARTESIAN_POINT ( 'NONE',  ( 1.559999999999998943, -1.732050807568885631, 0.000000000000000000 ) ) ;
#5182=CARTESIAN_POINT ( 'NONE',  ( 2.426025403784448642, 2.655529440325959183E-32, -2.168404344971008868E-16 ) ) ;
#5194=ORIENTED_EDGE ( 'NONE', *, *, #4185, .F. ) ;
#5221=DIRECTION ( 'NONE',  ( -1.000000000000000000, 0.000000000000000000, 0.000000000000000000 ) ) ;
#5295=CARTESIAN_POINT ( 'NONE',  ( 27.30499999999999616, 0.000000000000000000, 0.000000000000000000 ) ) ;
#5315=FACE_OUTER_BOUND ( 'NONE', #7371, .T. ) ;
#5332=CARTESIAN_POINT ( 'NONE',  ( 0.000000000000000000, 0.000000000000000000, 0.000000000000000000 ) ) ;
#5351=TOROIDAL_SURFACE ( 'NONE', #1396, 2.699999999999999289, 0.2000000000000000111 ) ;
#5369=ORIENTED_EDGE ( 'NONE', *, *, #11224, .F. ) ;
#5376=AXIS2_PLACEMENT_3D ( 'NONE', #12829, #1944, #3005 ) ;
#5410=CARTESIAN_POINT ( 'NONE',  ( 0.000000000000000000, 0.000000000000000000, 2.499999999999999112 ) ) ;
#5435=DIRECTION ( 'NONE',  ( 0.000000000000000000, 0.000000000000000000, 1.000000000000000000 ) ) ;
#5441=ORIENTED_EDGE ( 'NONE', *, *, #6741, .F. ) ;
#5482=CARTESIAN_POINT ( 'NONE',  ( 0.000000000000000000, 0.000000000000000000, 0.000000000000000000 ) ) ;
#5569=VECTOR ( 'NONE', #5221, 1000.000000000000000 ) ;
#5606=DIRECTION ( 'NONE',  ( -1.000000000000000000, 0.000000000000000000, 0.000000000000000000 ) ) ;
#5609=ORIENTED_EDGE ( 'NONE', *, *, #11549, .F. ) ;
#5631=CARTESIAN_POINT ( 'NONE',  ( 1.559999999999998943, -0.8660254037844428154, 1.500000000000001332 ) ) ;
#5649=DIRECTION ( 'NONE',  ( 0.000000000000000000, 0.000000000000000000, 1.000000000000000000 ) ) ;
#5667=CARTESIAN_POINT ( 'NONE',  ( 0.000000000000000000, -1.732050807568885631, 0.000000000000000000 ) ) ;
#5669=DIRECTION ( 'NONE',  ( -1.000000000000000000, 0.000000000000000000, 0.000000000000000000 ) ) ;
#5681=ORIENTED_EDGE ( 'NONE', *, *, #12902, .F. ) ;
#5691=LINE ( 'NONE', #9746, #15966 ) ;
#5706=DIRECTION ( 'NONE',  ( 1.000000000000000000, 0.000000000000000000, 0.000000000000000000 ) ) ;
#5748=DIRECTION ( 'NONE',  ( -1.000000000000000000, 0.000000000000000000, 0.000000000000000000 ) ) ;
#5759=EDGE_CURVE ( 'NONE', #1219, #6587, #11534, .T. ) ;
#5774=EDGE_LOOP ( 'NONE', ( #17206, #7594, #7139, #11187, #378 ) ) ;
#5800=EDGE_LOOP ( 'NONE', ( #891, #9210, #13059, #12007 ) ) ;
#5831=CIRCLE ( 'NONE', #6702, 2.499999999999999556 ) ;
#5870=VERTEX_POINT ( 'NONE', #15683 ) ;
#5873=DIRECTION ( 'NONE',  ( 0.000000000000000000, 0.000000000000000000, 1.000000000000000000 ) ) ;
#5885=ADVANCED_FACE ( 'NONE', ( #14276 ), #4976, .T. ) ;
#5898=DIRECTION ( 'NONE',  ( 0.000000000000000000, 0.000000000000000000, 1.000000000000000000 ) ) ;
#5900=ORIENTED_EDGE ( 'NONE', *, *, #2398, .T. ) ;
#5924=CARTESIAN_POINT ( 'NONE',  ( 1.559999999999998943, -0.8660254037844428154, 1.500000000000001332 ) ) ;
#5932=AXIS2_PLACEMENT_3D ( 'NONE', #645, #11085, #11433 ) ;
#5970=LINE ( 'NONE', #16685, #9309 ) ;
#6030=DIRECTION ( 'NONE',  ( 0.000000000000000000, 0.000000000000000000, -1.000000000000000000 ) ) ;
#6044=ORIENTED_EDGE ( 'NONE', *, *, #13788, .T. ) ;
#6053=CARTESIAN_POINT ( 'NONE',  ( 1.559999999999998943, 0.000000000000000000, 1.500000000000001332 ) ) ;
#6073=VECTOR ( 'NONE', #6119, 1000.000000000000000 ) ;
#6080=EDGE_CURVE ( 'NONE', #16562, #7137, #5831, .T. ) ;
#6084=VECTOR ( 'NONE', #11950, 1000.000000000000114 ) ;
#6116=CARTESIAN_POINT ( 'NONE',  ( 1.559999999999998943, -1.732050807568885631, 0.000000000000000000 ) ) ;
#6119=DIRECTION ( 'NONE',  ( 0.000000000000000000, -1.000000000000000000, 0.000000000000000000 ) ) ;
#6124=DIRECTION ( 'NONE',  ( 0.000000000000000000, -0.4999999999999996114, -0.8660254037844388186 ) ) ;
#6217=AXIS2_PLACEMENT_3D ( 'NONE', #16383, #4423, #12214 ) ;
#6223=VECTOR ( 'NONE', #15296, 1000.000000000000000 ) ;
#6245=SURFACE_STYLE_FILL_AREA ( #6413 ) ;
#6255=ADVANCED_FACE ( 'NONE', ( #8422 ), #7364, .F. ) ;
#6268=ADVANCED_FACE ( 'NONE', ( #3113 ), #8777, .F. ) ;
#6285=DIRECTION ( 'NONE',  ( 0.000000000000000000, 0.000000000000000000, 1.000000000000000000 ) ) ;
#6301=ORIENTED_EDGE ( 'NONE', *, *, #7385, .T. ) ;
#6326=ORIENTED_EDGE ( 'NONE', *, *, #6959, .F. ) ;
#6338=CIRCLE ( 'NONE', #7479, 2.055000000000000160 ) ;
#6348=ORIENTED_EDGE ( 'NONE', *, *, #12515, .F. ) ;
#6379=CARTESIAN_POINT ( 'NONE',  ( 1.559999999999998943, -0.8660254037844428154, 1.500000000000001332 ) ) ;
#6385=EDGE_CURVE ( 'NONE', #2044, #12997, #3294, .T. ) ;
#6413=FILL_AREA_STYLE ('',( #10566 ) ) ;
#6421=ORIENTED_EDGE ( 'NONE', *, *, #9625, .T. ) ;
#6429=ORIENTED_EDGE ( 'NONE', *, *, #16758, .F. ) ;
#6435=FILL_AREA_STYLE_COLOUR ( '', #2463 ) ;
#6446=CARTESIAN_POINT ( 'NONE',  ( 0.000000000000000000, -0.8660254037844428154, 1.500000000000001332 ) ) ;
#6450=VECTOR ( 'NONE', #10575, 1000.000000000000114 ) ;
#6467=FACE_OUTER_BOUND ( 'NONE', #9282, .T. ) ;
#6528=EDGE_CURVE ( 'NONE', #16562, #4758, #16211, .T. ) ;
#6546=ORIENTED_EDGE ( 'NONE', *, *, #6992, .T. ) ;
#6585=SHAPE_REPRESENTATION ( 'socket button head screw_iso_ISO 7380 - M5 x 25 - 25N', ( #3583 ), #14620 ) ;
#6587=VERTEX_POINT ( 'NONE', #9636 ) ;
#6621=AXIS2_PLACEMENT_3D ( 'NONE', #5295, #10857, #9438 ) ;
#6677=EDGE_CURVE ( 'NONE', #12789, #13912, #8102, .T. ) ;
#6678=ORIENTED_EDGE ( 'NONE', *, *, #2398, .F. ) ;
#6691=DIRECTION ( 'NONE',  ( 0.000000000000000000, 0.000000000000000000, 1.000000000000000000 ) ) ;
#6701=CIRCLE ( 'NONE', #3873, 1.500000000000000000 ) ;
#6702=AXIS2_PLACEMENT_3D ( 'NONE', #9657, #1261, #8326 ) ;
#6708=CARTESIAN_POINT ( 'NONE',  ( 2.950000000000001066, 0.000000000000000000, 2.699999999999999289 ) ) ;
#6725=CIRCLE ( 'NONE', #10674, 1.500000000000000000 ) ;
#6741=EDGE_CURVE ( 'NONE', #4376, #10086, #13978, .T. ) ;
#6781=VECTOR ( 'NONE', #15772, 1000.000000000000114 ) ;
#6810=ORIENTED_EDGE ( 'NONE', *, *, #5092, .T. ) ;
#6811=FACE_OUTER_BOUND ( 'NONE', #11939, .T. ) ;
#6857=DIRECTION ( 'NONE',  ( 1.000000000000000000, -0.000000000000000000, -0.000000000000000000 ) ) ;
#6893=DIRECTION ( 'NONE',  ( 0.000000000000000000, 0.000000000000000000, 1.000000000000000000 ) ) ;
#6895=CARTESIAN_POINT ( 'NONE',  ( 2.370000000000000551, 0.000000000000000000, 0.000000000000000000 ) ) ;
#6936=EDGE_CURVE ( 'NONE', #8817, #9579, #694, .T. ) ;
#6959=EDGE_CURVE ( 'NONE', #7137, #16562, #12554, .T. ) ;
#6966=ORIENTED_EDGE ( 'NONE', *, *, #8341, .F. ) ;
#6982=ORIENTED_EDGE ( 'NONE', *, *, #15307, .T. ) ;
#6992=EDGE_CURVE ( 'NONE', #8731, #6587, #15176, .T. ) ;
#6996=AXIS2_PLACEMENT_3D ( 'NONE', #2823, #13629, #13900 ) ;
#7011=CARTESIAN_POINT ( 'NONE',  ( 1.559999999999998943, 1.732050807568885631, 0.000000000000000000 ) ) ;
#7028=ORIENTED_EDGE ( 'NONE', *, *, #11898, .F. ) ;
#7100=DIRECTION ( 'NONE',  ( 1.000000000000000000, 0.000000000000000000, 0.000000000000000000 ) ) ;
#7137=VERTEX_POINT ( 'NONE', #8717 ) ;
#7139=ORIENTED_EDGE ( 'NONE', *, *, #11898, .T. ) ;
#7174=DIRECTION ( 'NONE',  ( 0.000000000000000000, 0.000000000000000000, 1.000000000000000000 ) ) ;
#7179=DIRECTION ( 'NONE',  ( 0.000000000000000000, 0.000000000000000000, -1.000000000000000000 ) ) ;
#7181=DIRECTION ( 'NONE',  ( -1.000000000000000000, 0.000000000000000000, 0.000000000000000000 ) ) ;
#7196=PLANE ( 'NONE',  #10730 ) ;
#7209=EDGE_CURVE ( 'NONE', #903, #118, #6338, .T. ) ;
#7215=CARTESIAN_POINT ( 'NONE',  ( 1.559999999999998943, 0.000000000000000000, 0.000000000000000000 ) ) ;
#7225=VECTOR ( 'NONE', #3251, 1000.000000000000114 ) ;
#7253=LINE ( 'NONE', #4606, #12405 ) ;
#7256=ORIENTED_EDGE ( 'NONE', *, *, #6677, .T. ) ;
#7257=ORIENTED_EDGE ( 'NONE', *, *, #2055, .T. ) ;
#7260=DIRECTION ( 'NONE',  ( 1.000000000000000000, 0.000000000000000000, 0.000000000000000000 ) ) ;
#7263=( GEOMETRIC_REPRESENTATION_CONTEXT ( 3 ) GLOBAL_UNCERTAINTY_ASSIGNED_CONTEXT ( ( #13687 ) ) GLOBAL_UNIT_ASSIGNED_CONTEXT ( ( #15973, #14476, #10388 ) ) REPRESENTATION_CONTEXT ( 'NONE', 'WORKASPACE' ) );
#7267=DIRECTION ( 'NONE',  ( 0.000000000000000000, -1.224646799147353207E-16, 1.000000000000000000 ) ) ;
#7280=DIRECTION ( 'NONE',  ( 0.000000000000000000, 0.5000000000000011102, -0.8660254037844379305 ) ) ;
#7288=ORIENTED_EDGE ( 'NONE', *, *, #12863, .T. ) ;
#7314=EDGE_CURVE ( 'NONE', #15354, #5870, #5691, .T. ) ;
#7318=VECTOR ( 'NONE', #11925, 1000.000000000000114 ) ;
#7337=EDGE_CURVE ( 'NONE', #9311, #8718, #9840, .T. ) ;
#7360=CARTESIAN_POINT ( 'NONE',  ( 2.950000000000001066, 3.306546357697852747E-16, -2.699999999999999289 ) ) ;
#7364=PLANE ( 'NONE',  #2728 ) ;
#7368=LINE ( 'NONE', #13926, #12284 ) ;
#7371=EDGE_LOOP ( 'NONE', ( #2952, #442, #6421, #12195, #15616 ) ) ;
#7385=EDGE_CURVE ( 'NONE', #4882, #13912, #7443, .T. ) ;
#7409=CYLINDRICAL_SURFACE ( 'NONE', #15195, 2.499999999999999112 ) ;
#7429=EDGE_CURVE ( 'NONE', #10063, #9579, #7368, .T. ) ;
#7443=LINE ( 'NONE', #16673, #15394 ) ;
#7479=AXIS2_PLACEMENT_3D ( 'NONE', #1450, #5606, #13659 ) ;
#7533=ORIENTED_EDGE ( 'NONE', *, *, #4116, .T. ) ;
#7594=ORIENTED_EDGE ( 'NONE', *, *, #11549, .T. ) ;
#7614=CARTESIAN_POINT ( 'NONE',  ( 27.75000000000000000, 0.000000000000000000, 0.000000000000000000 ) ) ;
#7622=CARTESIAN_POINT ( 'NONE',  ( 0.000000000000000000, -1.732050807568885631, 0.000000000000000000 ) ) ;
#7643=AXIS2_PLACEMENT_3D ( 'NONE', #1735, #9777, #11189 ) ;
#7703=ORIENTED_EDGE ( 'NONE', *, *, #7337, .F. ) ;
#7738=EDGE_CURVE ( 'NONE', #9579, #8740, #12434, .T. ) ;
#7755=VECTOR ( 'NONE', #10576, 1000.000000000000000 ) ;
#7794=PLANE ( 'NONE',  #2161 ) ;
#7844=ADVANCED_FACE ( 'NONE', ( #16741 ), #1417, .F. ) ;
#7871=ORIENTED_EDGE ( 'NONE', *, *, #15095, .T. ) ;
#7900=EDGE_LOOP ( 'NONE', ( #4616, #16565 ) ) ;
#7969=LINE ( 'NONE', #3810, #472 ) ;
#7976=ORIENTED_EDGE ( 'NONE', *, *, #2055, .F. ) ;
#8008=ORIENTED_EDGE ( 'NONE', *, *, #10013, .T. ) ;
#8014=EDGE_LOOP ( 'NONE', ( #10910, #17360, #17038, #1982 ) ) ;
#8018=VERTEX_POINT ( 'NONE', #6446 ) ;
#8024=AXIS2_PLACEMENT_3D ( 'NONE', #10073, #5669, #9904 ) ;
#8030=LINE ( 'NONE', #14683, #13563 ) ;
#8047=DIRECTION ( 'NONE',  ( -1.000000000000000000, 0.000000000000000000, 0.000000000000000000 ) ) ;
#8052=CARTESIAN_POINT ( 'NONE',  ( 2.750000000000000000, 3.306546357697852747E-16, -2.699999999999999289 ) ) ;
#8054=DIRECTION ( 'NONE',  ( -1.000000000000000000, 0.000000000000000000, 0.000000000000000000 ) ) ;
#8102=CIRCLE ( 'NONE', #121, 1.500000000000000000 ) ;
#8105=MECHANICAL_DESIGN_GEOMETRIC_PRESENTATION_REPRESENTATION('',(#13501),#7263);
#8117=( GEOMETRIC_REPRESENTATION_CONTEXT ( 3 ) GLOBAL_UNCERTAINTY_ASSIGNED_CONTEXT ( ( #5086 ) ) GLOBAL_UNIT_ASSIGNED_CONTEXT ( ( #16360, #2972, #13614 ) ) REPRESENTATION_CONTEXT ( 'NONE', 'WORKASPACE' ) );
#8126=FACE_OUTER_BOUND ( 'NONE', #7900, .T. ) ;
#8135=EDGE_CURVE ( 'NONE', #118, #7137, #17425, .T. ) ;
#8145=AXIS2_PLACEMENT_3D ( 'NONE', #6895, #12292, #15116 ) ;
#8169=VECTOR ( 'NONE', #7280, 1000.000000000000114 ) ;
#8207=VECTOR ( 'NONE', #440, 1000.000000000000000 ) ;
#8211=EDGE_LOOP ( 'NONE', ( #8008, #3719, #7288, #2312, #6966 ) ) ;
#8222=DIRECTION ( 'NONE',  ( 1.000000000000000000, 0.000000000000000000, 0.000000000000000000 ) ) ;
#8230=CARTESIAN_POINT ( 'NONE',  ( 2.950000000000001066, 0.000000000000000000, 0.000000000000000000 ) ) ;
#8326=DIRECTION ( 'NONE',  ( 0.000000000000000000, 0.000000000000000000, 1.000000000000000000 ) ) ;
#8341=EDGE_CURVE ( 'NONE', #10145, #5870, #9892, .T. ) ;
#8361=CARTESIAN_POINT ( 'NONE',  ( 0.000000000000000000, -0.8660254037844428154, 1.500000000000001332 ) ) ;
#8364=PRODUCT_DEFINITION_CONTEXT ( 'detailed design', #86, 'design' ) ;
#8382=FACE_OUTER_BOUND ( 'NONE', #4345, .T. ) ;
#8406=EDGE_CURVE ( 'NONE', #2141, #10037, #15899, .T. ) ;
#8415=DIRECTION ( 'NONE',  ( -1.000000000000000000, 0.000000000000000000, 0.000000000000000000 ) ) ;
#8422=FACE_OUTER_BOUND ( 'NONE', #2647, .T. ) ;
#8431=EDGE_LOOP ( 'NONE', ( #12713, #6982, #4399, #6348, #7976 ) ) ;
#8487=CIRCLE ( 'NONE', #10752, 1.500000000000000000 ) ;
#8520=EDGE_LOOP ( 'NONE', ( #11795, #4134, #12539 ) ) ;
#8542=LINE ( 'NONE', #8361, #818 ) ;
#8549=ORIENTED_EDGE ( 'NONE', *, *, #12704, .F. ) ;
#8584=DIRECTION ( 'NONE',  ( 0.000000000000000000, -0.000000000000000000, 1.000000000000000000 ) ) ;
#8634=CARTESIAN_POINT ( 'NONE',  ( 1.559999999999998943, 0.8660254037844428154, 1.500000000000001332 ) ) ;
#8660=LINE ( 'NONE', #5924, #12346 ) ;
#8680=CIRCLE ( 'NONE', #16885, 2.499999999999999112 ) ;
#8695=AXIS2_PLACEMENT_3D ( 'NONE', #6708, #13522, #13789 ) ;
#8717=CARTESIAN_POINT ( 'NONE',  ( 27.30499999999999616, 3.061616997868382648E-16, -2.499999999999999556 ) ) ;
#8718=VERTEX_POINT ( 'NONE', #5631 ) ;
#8731=VERTEX_POINT ( 'NONE', #1552 ) ;
#8734=CIRCLE ( 'NONE', #14658, 2.055000000000000160 ) ;
#8735=DIRECTION ( 'NONE',  ( 0.000000000000000000, 0.000000000000000000, -1.000000000000000000 ) ) ;
#8740=VERTEX_POINT ( 'NONE', #482 ) ;
#8777=PLANE ( 'NONE',  #2162 ) ;
#8783=ADVANCED_FACE ( 'NONE', ( #13951 ), #15179, .T. ) ;
#8786=CARTESIAN_POINT ( 'NONE',  ( 1.559999999999998943, 1.732050807568885631, 0.000000000000000000 ) ) ;
#8817=VERTEX_POINT ( 'NONE', #10126 ) ;
#8856=EDGE_LOOP ( 'NONE', ( #10763, #3110 ) ) ;
#8881=AXIS2_PLACEMENT_3D ( 'NONE', #10890, #1440, #12574 ) ;
#8891=CONICAL_SURFACE ( 'NONE', #9756, 2.055000000000000160, 0.7853981633974428389 ) ;
#8931=VERTEX_POINT ( 'NONE', #7011 ) ;
#8945=FACE_OUTER_BOUND ( 'NONE', #15779, .T. ) ;
#8970=DIRECTION ( 'NONE',  ( 0.000000000000000000, 0.000000000000000000, 1.000000000000000000 ) ) ;
#9009=CARTESIAN_POINT ( 'NONE',  ( 1.559999999999998943, -0.8660254037844428154, -1.499999999999997780 ) ) ;
#9053=CARTESIAN_POINT ( 'NONE',  ( 2.950000000000001066, 0.000000000000000000, 0.000000000000000000 ) ) ;
#9100=ADVANCED_FACE ( 'NONE', ( #2876 ), #2620, .T. ) ;
#9131=DIRECTION ( 'NONE',  ( 0.000000000000000000, 0.8660254037844380415, 0.5000000000000011102 ) ) ;
#9210=ORIENTED_EDGE ( 'NONE', *, *, #6385, .F. ) ;
#9214=DIRECTION ( 'NONE',  ( -1.000000000000000000, 0.000000000000000000, 0.000000000000000000 ) ) ;
#9255=PRODUCT_DEFINITION_FORMATION_WITH_SPECIFIED_SOURCE ( 'ANY', '', #4183, .NOT_KNOWN. ) ;
#9282=EDGE_LOOP ( 'NONE', ( #4440, #9663, #11600, #5369 ) ) ;
#9287=CARTESIAN_POINT ( 'NONE',  ( 0.000000000000000000, 0.8660254037844428154, -1.499999999999997780 ) ) ;
#9302=EDGE_LOOP ( 'NONE', ( #13324, #11398, #1049, #12552, #14493 ) ) ;
#9304=DIRECTION ( 'NONE',  ( 1.000000000000000000, 0.000000000000000000, 0.000000000000000000 ) ) ;
#9305=AXIS2_PLACEMENT_3D ( 'NONE', #6379, #4883, #11778 ) ;
#9309=VECTOR ( 'NONE', #4374, 1000.000000000000000 ) ;
#9311=VERTEX_POINT ( 'NONE', #6053 ) ;
#9351=ORIENTED_EDGE ( 'NONE', *, *, #15095, .F. ) ;
#9357=SURFACE_STYLE_USAGE ( .BOTH. , #16095 ) ;
#9394=FACE_OUTER_BOUND ( 'NONE', #8520, .T. ) ;
#9438=DIRECTION ( 'NONE',  ( 0.000000000000000000, 0.000000000000000000, 1.000000000000000000 ) ) ;
#9513=DIRECTION ( 'NONE',  ( -1.000000000000000000, 0.000000000000000000, 0.000000000000000000 ) ) ;
#9527=CARTESIAN_POINT ( 'NONE',  ( 4.755015822784812052, 0.000000000000000000, 0.000000000000000000 ) ) ;
#9533=DIRECTION ( 'NONE',  ( -1.000000000000000000, 0.000000000000000000, 0.000000000000000000 ) ) ;
#9559=EDGE_LOOP ( 'NONE', ( #5609, #13165, #7256, #2030, #2694 ) ) ;
#9573=CARTESIAN_POINT ( 'NONE',  ( 0.000000000000000000, 0.000000000000000000, 4.750000000000000000 ) ) ;
#9579=VERTEX_POINT ( 'NONE', #1522 ) ;
#9587=ORIENTED_EDGE ( 'NONE', *, *, #6528, .F. ) ;
#9596=VECTOR ( 'NONE', #15404, 1000.000000000000114 ) ;
#9623=CARTESIAN_POINT ( 'NONE',  ( 1.559999999999998943, -1.732050807568885631, 0.000000000000000000 ) ) ;
#9625=EDGE_CURVE ( 'NONE', #1652, #374, #11973, .T. ) ;
#9636=CARTESIAN_POINT ( 'NONE',  ( 0.000000000000000000, 0.8660254037844428154, 1.500000000000001332 ) ) ;
#9642=CARTESIAN_POINT ( 'NONE',  ( 1.559999999999998943, 0.8660254037844428154, 1.500000000000001332 ) ) ;
#9657=CARTESIAN_POINT ( 'NONE',  ( 27.30499999999999616, 0.000000000000000000, 0.000000000000000000 ) ) ;
#9663=ORIENTED_EDGE ( 'NONE', *, *, #8135, .T. ) ;
#9724=LINE ( 'NONE', #16473, #198 ) ;
#9744=CARTESIAN_POINT ( 'NONE',  ( 1.559999999999998943, -1.732050807568885631, 0.000000000000000000 ) ) ;
#9746=CARTESIAN_POINT ( 'NONE',  ( 0.000000000000000000, -0.8660254037844428154, -1.499999999999997780 ) ) ;
#9753=ORIENTED_EDGE ( 'NONE', *, *, #10259, .F. ) ;
#9756=AXIS2_PLACEMENT_3D ( 'NONE', #11157, #7181, #550 ) ;
#9777=DIRECTION ( 'NONE',  ( 0.000000000000000000, 0.8660254037844380415, -0.5000000000000012212 ) ) ;
#9840=LINE ( 'NONE', #11159, #6073 ) ;
#9877=ORIENTED_EDGE ( 'NONE', *, *, #6677, .F. ) ;
#9892=LINE ( 'NONE', #2984, #6223 ) ;
#9904=DIRECTION ( 'NONE',  ( 0.000000000000000000, 0.000000000000000000, 1.000000000000000000 ) ) ;
#9934=CARTESIAN_POINT ( 'NONE',  ( 1.559999999999998943, -0.8660254037844428154, -1.499999999999997780 ) ) ;
#9982=ORIENTED_EDGE ( 'NONE', *, *, #1384, .T. ) ;
#9986=DIRECTION ( 'NONE',  ( 0.000000000000000000, -0.8660254037844388186, -0.4999999999999998335 ) ) ;
#10013=EDGE_CURVE ( 'NONE', #10145, #12789, #7253, .T. ) ;
#10030=VECTOR ( 'NONE', #2564, 1000.000000000000000 ) ;
#10037=VERTEX_POINT ( 'NONE', #4688 ) ;
#10063=VERTEX_POINT ( 'NONE', #10170 ) ;
#10073=CARTESIAN_POINT ( 'NONE',  ( 0.000000000000000000, 0.000000000000000000, 0.000000000000000000 ) ) ;
#10074=AXIS2_PLACEMENT_3D ( 'NONE', #14316, #3438, #4596 ) ;
#10086=VERTEX_POINT ( 'NONE', #16816 ) ;
#10087=DIRECTION ( 'NONE',  ( 0.000000000000000000, 0.000000000000000000, 1.000000000000000000 ) ) ;
#10102=ORIENTED_EDGE ( 'NONE', *, *, #5092, .F. ) ;
#10118=DIRECTION ( 'NONE',  ( 0.000000000000000000, -0.5000000000000011102, -0.8660254037844379305 ) ) ;
#10126=CARTESIAN_POINT ( 'NONE',  ( 2.370000000000000551, 4.750000000000000888, 0.000000000000000000 ) ) ;
#10145=VERTEX_POINT ( 'NONE', #9009 ) ;
#10170=CARTESIAN_POINT ( 'NONE',  ( 2.749999999999999112, 5.817072295949927426E-16, -4.750000000000000000 ) ) ;
#10233=CARTESIAN_POINT ( 'NONE',  ( 2.950000000000001066, 3.061616997868382155E-16, -2.499999999999999112 ) ) ;
#10237=CARTESIAN_POINT ( 'NONE',  ( 2.749999999999999112, 0.000000000000000000, 0.000000000000000000 ) ) ;
#10258=ORIENTED_EDGE ( 'NONE', *, *, #6080, .T. ) ;
#10259=EDGE_CURVE ( 'NONE', #12789, #2141, #8030, .T. ) ;
#10270=CARTESIAN_POINT ( 'NONE',  ( 4.755015822784812052, 0.000000000000000000, 0.000000000000000000 ) ) ;
#10358=SPHERICAL_SURFACE ( 'NONE', #11541, 5.315148208181398104 ) ;
#10362=FACE_BOUND ( 'NONE', #15397, .T. ) ;
#10366=DIRECTION ( 'NONE',  ( -1.000000000000000000, 0.000000000000000000, 0.000000000000000000 ) ) ;
#10388=( NAMED_UNIT ( * ) SI_UNIT ( $, .STERADIAN. ) SOLID_ANGLE_UNIT ( ) );
#10447=LINE ( 'NONE', #2126, #6084 ) ;
#10458=FACE_OUTER_BOUND ( 'NONE', #17301, .T. ) ;
#10465=ADVANCED_FACE ( 'NONE', ( #8382 ), #1668, .F. ) ;
#10494=DIRECTION ( 'NONE',  ( 0.000000000000000000, 0.4999999999999996669, 0.8660254037844388186 ) ) ;
#10522=DIRECTION ( 'NONE',  ( -1.000000000000000000, 0.000000000000000000, 0.000000000000000000 ) ) ;
#10566=FILL_AREA_STYLE_COLOUR ( '', #11506 ) ;
#10575=DIRECTION ( 'NONE',  ( -0.5000000000000042188, 1.060575238724903710E-16, -0.8660254037844361541 ) ) ;
#10576=DIRECTION ( 'NONE',  ( 0.000000000000000000, 1.000000000000000000, 0.000000000000000000 ) ) ;
#10607=ORIENTED_EDGE ( 'NONE', *, *, #1255, .F. ) ;
#10648=EDGE_CURVE ( 'NONE', #5870, #2623, #13247, .T. ) ;
#10654=ORIENTED_EDGE ( 'NONE', *, *, #8341, .T. ) ;
#10659=ORIENTED_EDGE ( 'NONE', *, *, #4185, .T. ) ;
#10674=AXIS2_PLACEMENT_3D ( 'NONE', #4063, #9533, #14937 ) ;
#10685=SURFACE_STYLE_FILL_AREA ( #2449 ) ;
#10709=CYLINDRICAL_SURFACE ( 'NONE', #15490, 4.750000000000000000 ) ;
#10717=FACE_OUTER_BOUND ( 'NONE', #12232, .T. ) ;
#10730=AXIS2_PLACEMENT_3D ( 'NONE', #2868, #5873, #5706 ) ;
#10752=AXIS2_PLACEMENT_3D ( 'NONE', #15452, #10366, #5898 ) ;
#10763=ORIENTED_EDGE ( 'NONE', *, *, #7209, .F. ) ;
#10835=ORIENTED_EDGE ( 'NONE', *, *, #7314, .T. ) ;
#10857=DIRECTION ( 'NONE',  ( -1.000000000000000000, 0.000000000000000000, 0.000000000000000000 ) ) ;
#10876=DIRECTION ( 'NONE',  ( -1.000000000000000000, 0.000000000000000000, 0.000000000000000000 ) ) ;
#10890=CARTESIAN_POINT ( 'NONE',  ( 1.559999999999998943, -1.732050807568885631, 0.000000000000000000 ) ) ;
#10910=ORIENTED_EDGE ( 'NONE', *, *, #1384, .F. ) ;
#10966=CARTESIAN_POINT ( 'NONE',  ( 1.559999999999998943, 0.000000000000000000, 0.000000000000000000 ) ) ;
#11057=DIRECTION ( 'NONE',  ( 0.000000000000000000, -0.5000000000000011102, -0.8660254037844379305 ) ) ;
#11085=DIRECTION ( 'NONE',  ( -1.000000000000000000, 0.000000000000000000, 0.000000000000000000 ) ) ;
#11155=ADVANCED_FACE ( 'NONE', ( #13826 ), #13724, .T. ) ;
#11157=CARTESIAN_POINT ( 'NONE',  ( 27.75000000000000000, 0.000000000000000000, 0.000000000000000000 ) ) ;
#11159=CARTESIAN_POINT ( 'NONE',  ( 1.559999999999998943, -0.8660254037844428154, 1.500000000000001332 ) ) ;
#11187=ORIENTED_EDGE ( 'NONE', *, *, #303, .T. ) ;
#11189=DIRECTION ( 'NONE',  ( 0.000000000000000000, 0.5000000000000012212, 0.8660254037844380415 ) ) ;
#11224=EDGE_CURVE ( 'NONE', #903, #16562, #3892, .T. ) ;
#11253=FACE_OUTER_BOUND ( 'NONE', #4629, .T. ) ;
#11398=ORIENTED_EDGE ( 'NONE', *, *, #7429, .T. ) ;
#11423=CARTESIAN_POINT ( 'NONE',  ( 1.559999999999998943, -1.732050807568885631, 0.000000000000000000 ) ) ;
#11431=DIRECTION ( 'NONE',  ( 0.000000000000000000, 1.000000000000000000, 0.000000000000000000 ) ) ;
#11433=DIRECTION ( 'NONE',  ( 0.000000000000000000, 0.000000000000000000, 1.000000000000000000 ) ) ;
#11469=CARTESIAN_POINT ( 'NONE',  ( 4.755015822784812052, 0.000000000000000000, 0.000000000000000000 ) ) ;
#11491=EDGE_CURVE ( 'NONE', #10063, #1652, #4969, .T. ) ;
#11500=ORIENTED_EDGE ( 'NONE', *, *, #12920, .T. ) ;
#11506=COLOUR_RGB ( '', 0.72549020, 0.75294118, 0.79215686) ;
#11534=LINE ( 'NONE', #12695, #1586 ) ;
#11541=AXIS2_PLACEMENT_3D ( 'NONE', #10270, #5057, #11431 ) ;
#11545=VECTOR ( 'NONE', #15193, 1000.000000000000000 ) ;
#11549=EDGE_CURVE ( 'NONE', #11634, #9311, #17053, .T. ) ;
#11600=ORIENTED_EDGE ( 'NONE', *, *, #6080, .F. ) ;
#11612=PLANE ( 'NONE',  #9305 ) ;
#11629=ORIENTED_EDGE ( 'NONE', *, *, #10648, .T. ) ;
#11634=VERTEX_POINT ( 'NONE', #2442 ) ;
#11778=DIRECTION ( 'NONE',  ( -1.000000000000000000, 0.000000000000000000, 0.000000000000000000 ) ) ;
#11795=ORIENTED_EDGE ( 'NONE', *, *, #3884, .F. ) ;
#11830=PRODUCT_CONTEXT ( 'NONE', #4939, 'mechanical' ) ;
#11898=EDGE_CURVE ( 'NONE', #9311, #12797, #1588, .T. ) ;
#11925=DIRECTION ( 'NONE',  ( 0.000000000000000000, 0.4999999999999996669, 0.8660254037844388186 ) ) ;
#11939=EDGE_LOOP ( 'NONE', ( #10258, #13644, #13397, #9587 ) ) ;
#11950=DIRECTION ( 'NONE',  ( 0.000000000000000000, -0.4999999999999997224, 0.8660254037844387076 ) ) ;
#11973=LINE ( 'NONE', #9573, #15311 ) ;
#12007=ORIENTED_EDGE ( 'NONE', *, *, #77, .F. ) ;
#12070=EDGE_LOOP ( 'NONE', ( #9877, #13223, #9351 ) ) ;
#12119=CARTESIAN_POINT ( 'NONE',  ( 27.75000000000000000, 0.000000000000000000, 2.055000000000000160 ) ) ;
#12130=DIRECTION ( 'NONE',  ( 0.000000000000000000, 0.000000000000000000, 1.000000000000000000 ) ) ;
#12135=AXIS2_PLACEMENT_3D ( 'NONE', #11469, #8735, #598 ) ;
#12195=ORIENTED_EDGE ( 'NONE', *, *, #16740, .F. ) ;
#12212=CARTESIAN_POINT ( 'NONE',  ( 2.749999999999999112, 0.000000000000000000, 4.750000000000000000 ) ) ;
#12214=DIRECTION ( 'NONE',  ( 0.000000000000000000, 0.000000000000000000, 1.000000000000000000 ) ) ;
#12219=LINE ( 'NONE', #349, #5010 ) ;
#12232=EDGE_LOOP ( 'NONE', ( #12838, #14361, #9753 ) ) ;
#12274=CARTESIAN_POINT ( 'NONE',  ( 27.75000000000000000, 0.000000000000000000, 0.000000000000000000 ) ) ;
#12284=VECTOR ( 'NONE', #1788, 1000.000000000000000 ) ;
#12292=DIRECTION ( 'NONE',  ( -1.000000000000000000, 0.000000000000000000, 0.000000000000000000 ) ) ;
#12346=VECTOR ( 'NONE', #12553, 1000.000000000000000 ) ;
#12372=CARTESIAN_POINT ( 'NONE',  ( 0.000000000000000000, 0.000000000000000000, 0.000000000000000000 ) ) ;
#12375=PRODUCT_DEFINITION_SHAPE ( 'NONE', 'NONE',  #4491 ) ;
#12390=CARTESIAN_POINT ( 'NONE',  ( 1.559999999999998943, 0.000000000000000000, 0.000000000000000000 ) ) ;
#12391=DIRECTION ( 'NONE',  ( -1.000000000000000000, 0.000000000000000000, 0.000000000000000000 ) ) ;
#12395=CIRCLE ( 'NONE', #13258, 5.315148208181398104 ) ;
#12405=VECTOR ( 'NONE', #12917, 1000.000000000000000 ) ;
#12434=CIRCLE ( 'NONE', #17244, 4.750000000000000000 ) ;
#12450=VECTOR ( 'NONE', #4238, 1000.000000000000000 ) ;
#12451=ORIENTED_EDGE ( 'NONE', *, *, #6385, .T. ) ;
#12467=DIRECTION ( 'NONE',  ( 1.000000000000000000, 0.000000000000000000, 0.000000000000000000 ) ) ;
#12515=EDGE_CURVE ( 'NONE', #8018, #15354, #4254, .T. ) ;
#12539=ORIENTED_EDGE ( 'NONE', *, *, #15307, .F. ) ;
#12542=DIRECTION ( 'NONE',  ( 0.000000000000000000, 1.000000000000000000, 1.224646799147353207E-16 ) ) ;
#12552=ORIENTED_EDGE ( 'NONE', *, *, #3862, .F. ) ;
#12553=DIRECTION ( 'NONE',  ( 0.000000000000000000, -1.000000000000000000, 0.000000000000000000 ) ) ;
#12554=CIRCLE ( 'NONE', #6621, 2.499999999999999556 ) ;
#12574=DIRECTION ( 'NONE',  ( 0.000000000000000000, 0.000000000000000000, -1.000000000000000000 ) ) ;
#12594=ORIENTED_EDGE ( 'NONE', *, *, #6936, .T. ) ;
#12609=AXIS2_PLACEMENT_3D ( 'NONE', #10237, #868, #12901 ) ;
#12673=CIRCLE ( 'NONE', #5036, 1.500000000000000000 ) ;
#12683=ORIENTED_EDGE ( 'NONE', *, *, #6741, .T. ) ;
#12695=CARTESIAN_POINT ( 'NONE',  ( 1.559999999999998943, 0.8660254037844428154, 1.500000000000001332 ) ) ;
#12704=EDGE_CURVE ( 'NONE', #8718, #15454, #7969, .T. ) ;
#12713=ORIENTED_EDGE ( 'NONE', *, *, #12704, .T. ) ;
#12716=ADVANCED_FACE ( 'NONE', ( #10717 ), #15938, .F. ) ;
#12726=FACE_OUTER_BOUND ( 'NONE', #15831, .T. ) ;
#12787=DIRECTION ( 'NONE',  ( 1.000000000000000000, 0.000000000000000000, 0.000000000000000000 ) ) ;
#12789=VERTEX_POINT ( 'NONE', #15609 ) ;
#12797=VERTEX_POINT ( 'NONE', #659 ) ;
#12811=DIRECTION ( 'NONE',  ( 0.000000000000000000, 0.000000000000000000, 1.000000000000000000 ) ) ;
#12829=CARTESIAN_POINT ( 'NONE',  ( -997.5739745962155212, 0.000000000000000000, 0.000000000000000000 ) ) ;
#12838=ORIENTED_EDGE ( 'NONE', *, *, #1221, .F. ) ;
#12847=DIRECTION ( 'NONE',  ( 0.000000000000000000, 0.5000000000000011102, -0.8660254037844379305 ) ) ;
#12852=DIRECTION ( 'NONE',  ( 0.000000000000000000, -0.8660254037844388186, 0.4999999999999996114 ) ) ;
#12863=EDGE_CURVE ( 'NONE', #2141, #2623, #9724, .T. ) ;
#12901=DIRECTION ( 'NONE',  ( 0.000000000000000000, 0.000000000000000000, 1.000000000000000000 ) ) ;
#12902=EDGE_CURVE ( 'NONE', #7137, #13658, #12219, .T. ) ;
#12914=TOROIDAL_SURFACE ( 'NONE', #188, 2.699999999999999289, 0.2000000000000000111 ) ;
#12917=DIRECTION ( 'NONE',  ( 0.000000000000000000, 1.000000000000000000, 0.000000000000000000 ) ) ;
#12920=EDGE_CURVE ( 'NONE', #4758, #13658, #8680, .T. ) ;
#12986=CARTESIAN_POINT ( 'NONE',  ( 1.559999999999998943, 1.732050807568885631, 0.000000000000000000 ) ) ;
#12997=VERTEX_POINT ( 'NONE', #8052 ) ;
#13039=EDGE_LOOP ( 'NONE', ( #13252, #17005, #7257, #15571, #3733 ) ) ;
#13059=ORIENTED_EDGE ( 'NONE', *, *, #16978, .T. ) ;
#13105=DIRECTION ( 'NONE',  ( -1.000000000000000000, 0.000000000000000000, 0.000000000000000000 ) ) ;
#13144=AXIS2_PLACEMENT_3D ( 'NONE', #7614, #13105, #15667 ) ;
#13160=ORIENTED_EDGE ( 'NONE', *, *, #8135, .F. ) ;
#13165=ORIENTED_EDGE ( 'NONE', *, *, #13661, .T. ) ;
#13190=CONICAL_SURFACE ( 'NONE', #3015, 1732.050807568857181, 1.047197551196592746 ) ;
#13205=DIRECTION ( 'NONE',  ( 0.000000000000000000, 0.000000000000000000, 1.000000000000000000 ) ) ;
#13223=ORIENTED_EDGE ( 'NONE', *, *, #10013, .F. ) ;
#13247=LINE ( 'NONE', #17402, #7755 ) ;
#13252=ORIENTED_EDGE ( 'NONE', *, *, #16758, .T. ) ;
#13258=AXIS2_PLACEMENT_3D ( 'NONE', #9527, #14935, #12542 ) ;
#13298=ORIENTED_EDGE ( 'NONE', *, *, #14141, .F. ) ;
#13324=ORIENTED_EDGE ( 'NONE', *, *, #2681, .T. ) ;
#13380=CARTESIAN_POINT ( 'NONE',  ( 1.559999999999998943, -1.299038105676664223, 0.7500000000000006661 ) ) ;
#13397=ORIENTED_EDGE ( 'NONE', *, *, #77, .T. ) ;
#13416=ORIENTED_EDGE ( 'NONE', *, *, #14141, .T. ) ;
#13429=EDGE_CURVE ( 'NONE', #15454, #9311, #6725, .T. ) ;
#13438=ADVANCED_FACE ( 'NONE', ( #6811 ), #13441, .T. ) ;
#13441=CYLINDRICAL_SURFACE ( 'NONE', #3037, 2.499999999999999112 ) ;
#13474=EDGE_LOOP ( 'NONE', ( #5900, #6810, #1229, #1319, #3320 ) ) ;
#13501=STYLED_ITEM ( 'NONE', ( #17041 ), #4875 ) ;
#13522=DIRECTION ( 'NONE',  ( 0.000000000000000000, -1.000000000000000000, 0.000000000000000000 ) ) ;
#13547=ADVANCED_FACE ( 'NONE', ( #2088 ), #7409, .T. ) ;
#13563=VECTOR ( 'NONE', #2562, 1000.000000000000000 ) ;
#13614=( NAMED_UNIT ( * ) SI_UNIT ( $, .STERADIAN. ) SOLID_ANGLE_UNIT ( ) );
#13629=DIRECTION ( 'NONE',  ( -1.000000000000000000, 0.000000000000000000, 0.000000000000000000 ) ) ;
#13644=ORIENTED_EDGE ( 'NONE', *, *, #12902, .T. ) ;
#13658=VERTEX_POINT ( 'NONE', #10233 ) ;
#13659=DIRECTION ( 'NONE',  ( 0.000000000000000000, 0.000000000000000000, 1.000000000000000000 ) ) ;
#13661=EDGE_CURVE ( 'NONE', #11634, #12789, #15809, .T. ) ;
#13678=DIRECTION ( 'NONE',  ( -1.000000000000000000, 0.000000000000000000, 0.000000000000000000 ) ) ;
#13687=UNCERTAINTY_MEASURE_WITH_UNIT (LENGTH_MEASURE( 1.000000000000000082E-05 ), #15973, 'distance_accuracy_value', 'NONE');
#13724=PLANE ( 'NONE',  #15408 ) ;
#13784=MECHANICAL_DESIGN_GEOMETRIC_PRESENTATION_REPRESENTATION('',(#14076),#8117);
#13788=EDGE_CURVE ( 'NONE', #10037, #8931, #13950, .T. ) ;
#13789=DIRECTION ( 'NONE',  ( 0.000000000000000000, 0.000000000000000000, -1.000000000000000000 ) ) ;
#13791=EDGE_LOOP ( 'NONE', ( #12451, #9982 ) ) ;
#13826=FACE_OUTER_BOUND ( 'NONE', #13474, .T. ) ;
#13857=CARTESIAN_POINT ( 'NONE',  ( 2.750000000000000000, 0.000000000000000000, 2.699999999999999289 ) ) ;
#13900=DIRECTION ( 'NONE',  ( 0.000000000000000000, 0.000000000000000000, 1.000000000000000000 ) ) ;
#13912=VERTEX_POINT ( 'NONE', #2328 ) ;
#13913=ORIENTED_EDGE ( 'NONE', *, *, #8406, .T. ) ;
#13926=CARTESIAN_POINT ( 'NONE',  ( 0.000000000000000000, 5.817072295949927426E-16, -4.750000000000000000 ) ) ;
#13950=LINE ( 'NONE', #14128, #16363 ) ;
#13951=FACE_OUTER_BOUND ( 'NONE', #8431, .T. ) ;
#13963=( NAMED_UNIT ( * ) SI_UNIT ( $, .STERADIAN. ) SOLID_ANGLE_UNIT ( ) );
#13978=CIRCLE ( 'NONE', #8024, 2.375000000000000000 ) ;
#13998=DIRECTION ( 'NONE',  ( -1.000000000000000000, 0.000000000000000000, 0.000000000000000000 ) ) ;
#14076=STYLED_ITEM ( 'NONE', ( #2185 ), #16934 ) ;
#14097=CIRCLE ( 'NONE', #1068, 2.375000000000000000 ) ;
#14128=CARTESIAN_POINT ( 'NONE',  ( 1.559999999999998943, 1.732050807568885631, 0.000000000000000000 ) ) ;
#14141=EDGE_CURVE ( 'NONE', #10086, #4376, #14097, .T. ) ;
#14181=FACE_OUTER_BOUND ( 'NONE', #5800, .T. ) ;
#14184=LINE ( 'NONE', #1957, #9596 ) ;
#14268=FACE_OUTER_BOUND ( 'NONE', #13039, .T. ) ;
#14276=FACE_OUTER_BOUND ( 'NONE', #3376, .T. ) ;
#14313=ADVANCED_FACE ( 'NONE', ( #17092 ), #10358, .T. ) ;
#14316=CARTESIAN_POINT ( 'NONE',  ( 2.370000000000000551, 0.000000000000000000, 0.000000000000000000 ) ) ;
#14347=ADVANCED_FACE ( 'NONE', ( #8945 ), #14357, .T. ) ;
#14357=PLANE ( 'NONE',  #1943 ) ;
#14361=ORIENTED_EDGE ( 'NONE', *, *, #8406, .F. ) ;
#14476=( NAMED_UNIT ( * ) PLANE_ANGLE_UNIT ( ) SI_UNIT ( $, .RADIAN. ) );
#14493=ORIENTED_EDGE ( 'NONE', *, *, #9625, .F. ) ;
#14537=CARTESIAN_POINT ( 'NONE',  ( 1.559999999999998943, -0.8660254037844428154, -1.499999999999997780 ) ) ;
#14554=SURFACE_STYLE_USAGE ( .BOTH. , #17307 ) ;
#14587=AXIS2_PLACEMENT_3D ( 'NONE', #14537, #9131, #4890 ) ;
#14620=( GEOMETRIC_REPRESENTATION_CONTEXT ( 3 ) GLOBAL_UNCERTAINTY_ASSIGNED_CONTEXT ( ( #15500 ) ) GLOBAL_UNIT_ASSIGNED_CONTEXT ( ( #3160, #3500, #13963 ) ) REPRESENTATION_CONTEXT ( 'NONE', 'WORKASPACE' ) );
#14623=CARTESIAN_POINT ( 'NONE',  ( 1.559999999999998943, 0.000000000000000000, 0.000000000000000000 ) ) ;
#14658=AXIS2_PLACEMENT_3D ( 'NONE', #12274, #3071, #4232 ) ;
#14683=CARTESIAN_POINT ( 'NONE',  ( 1.559999999999998943, 0.8660254037844428154, -1.499999999999997780 ) ) ;
#14808=DIRECTION ( 'NONE',  ( 0.000000000000000000, 0.5000000000000011102, -0.8660254037844379305 ) ) ;
#14825=CARTESIAN_POINT ( 'NONE',  ( 0.000000000000000000, 0.000000000000000000, 0.000000000000000000 ) ) ;
#14864=CIRCLE ( 'NONE', #4130, 2.499999999999999112 ) ;
#14935=DIRECTION ( 'NONE',  ( 0.000000000000000000, 1.224646799147353207E-16, -1.000000000000000000 ) ) ;
#14937=DIRECTION ( 'NONE',  ( 0.000000000000000000, 0.000000000000000000, 1.000000000000000000 ) ) ;
#14943=PLANE ( 'NONE',  #6996 ) ;
#14964=ORIENTED_EDGE ( 'NONE', *, *, #13788, .F. ) ;
#14979=DIRECTION ( 'NONE',  ( -1.000000000000000000, 0.000000000000000000, 0.000000000000000000 ) ) ;
#15095=EDGE_CURVE ( 'NONE', #13912, #10145, #1972, .T. ) ;
#15116=DIRECTION ( 'NONE',  ( 0.000000000000000000, 0.000000000000000000, 1.000000000000000000 ) ) ;
#15132=ADVANCED_FACE ( 'NONE', ( #1716 ), #1625, .F. ) ;
#15176=LINE ( 'NONE', #1731, #16243 ) ;
#15179=PLANE ( 'NONE',  #7643 ) ;
#15193=DIRECTION ( 'NONE',  ( -1.000000000000000000, 0.000000000000000000, 0.000000000000000000 ) ) ;
#15195=AXIS2_PLACEMENT_3D ( 'NONE', #1832, #15464, #12811 ) ;
#15201=DIRECTION ( 'NONE',  ( 0.000000000000000000, 0.000000000000000000, -1.000000000000000000 ) ) ;
#15215=DIRECTION ( 'NONE',  ( -1.000000000000000000, 0.000000000000000000, 0.000000000000000000 ) ) ;
#15229=ADVANCED_FACE ( 'NONE', ( #14268 ), #11612, .T. ) ;
#15241=DIRECTION ( 'NONE',  ( 1.000000000000000000, 0.000000000000000000, 0.000000000000000000 ) ) ;
#15253=CARTESIAN_POINT ( 'NONE',  ( 2.950000000000001066, 0.000000000000000000, 0.000000000000000000 ) ) ;
#15296=DIRECTION ( 'NONE',  ( -1.000000000000000000, 0.000000000000000000, 0.000000000000000000 ) ) ;
#15307=EDGE_CURVE ( 'NONE', #15454, #4882, #3556, .T. ) ;
#15311=VECTOR ( 'NONE', #14979, 1000.000000000000000 ) ;
#15354=VERTEX_POINT ( 'NONE', #7622 ) ;
#15394=VECTOR ( 'NONE', #12847, 1000.000000000000114 ) ;
#15397=EDGE_LOOP ( 'NONE', ( #16783, #4830, #10835, #11629, #7533, #6546 ) ) ;
#15404=DIRECTION ( 'NONE',  ( 0.000000000000000000, -0.4999999999999997224, 0.8660254037844387076 ) ) ;
#15408=AXIS2_PLACEMENT_3D ( 'NONE', #9642, #9986, #4340 ) ;
#15452=CARTESIAN_POINT ( 'NONE',  ( 1.559999999999998943, 0.000000000000000000, 0.000000000000000000 ) ) ;
#15454=VERTEX_POINT ( 'NONE', #13380 ) ;
#15464=DIRECTION ( 'NONE',  ( -1.000000000000000000, 0.000000000000000000, 0.000000000000000000 ) ) ;
#15490=AXIS2_PLACEMENT_3D ( 'NONE', #1062, #8047, #12130 ) ;
#15500=UNCERTAINTY_MEASURE_WITH_UNIT (LENGTH_MEASURE( 1.000000000000000082E-05 ), #3160, 'distance_accuracy_value', 'NONE');
#15571=ORIENTED_EDGE ( 'NONE', *, *, #1862, .F. ) ;
#15609=CARTESIAN_POINT ( 'NONE',  ( 1.559999999999998943, 0.000000000000000000, -1.499999999999997780 ) ) ;
#15616=ORIENTED_EDGE ( 'NONE', *, *, #7738, .F. ) ;
#15665=DIRECTION ( 'NONE',  ( -1.000000000000000000, 0.000000000000000000, 0.000000000000000000 ) ) ;
#15667=DIRECTION ( 'NONE',  ( 0.000000000000000000, 0.000000000000000000, 1.000000000000000000 ) ) ;
#15683=CARTESIAN_POINT ( 'NONE',  ( 0.000000000000000000, -0.8660254037844428154, -1.499999999999997780 ) ) ;
#15772=DIRECTION ( 'NONE',  ( 0.000000000000000000, -0.5000000000000011102, -0.8660254037844379305 ) ) ;
#15773=PLANE ( 'NONE',  #17434 ) ;
#15779=EDGE_LOOP ( 'NONE', ( #13913, #6044, #2420, #3369, #3801 ) ) ;
#15809=LINE ( 'NONE', #5182, #6450 ) ;
#15831=EDGE_LOOP ( 'NONE', ( #5194, #2001, #307, #4019, #5441 ) ) ;
#15899=LINE ( 'NONE', #12986, #4263 ) ;
#15935=CARTESIAN_POINT ( 'NONE',  ( 2.749999999999999112, 0.000000000000000000, 0.000000000000000000 ) ) ;
#15938=PLANE ( 'NONE',  #4995 ) ;
#15966=VECTOR ( 'NONE', #14808, 1000.000000000000114 ) ;
#15973=( LENGTH_UNIT ( ) NAMED_UNIT ( * ) SI_UNIT ( .MILLI., .METRE. ) );
#15999=LINE ( 'NONE', #151, #11545 ) ;
#16001=DIRECTION ( 'NONE',  ( -1.000000000000000000, 0.000000000000000000, 0.000000000000000000 ) ) ;
#16094=ORIENTED_EDGE ( 'NONE', *, *, #6528, .T. ) ;
#16095=SURFACE_SIDE_STYLE ('',( #10685 ) ) ;
#16211=LINE ( 'NONE', #5410, #5569 ) ;
#16243=VECTOR ( 'NONE', #388, 1000.000000000000114 ) ;
#16272=CARTESIAN_POINT ( 'NONE',  ( 2.370000000000000551, 0.000000000000000000, 0.000000000000000000 ) ) ;
#16295=DIRECTION ( 'NONE',  ( 1.000000000000000000, -0.000000000000000000, -0.000000000000000000 ) ) ;
#16306=CARTESIAN_POINT ( 'NONE',  ( 2.370000000000000551, 0.000000000000000000, 4.750000000000000000 ) ) ;
#16317=ADVANCED_FACE ( 'NONE', ( #1607 ), #4346, .F. ) ;
#16360=( LENGTH_UNIT ( ) NAMED_UNIT ( * ) SI_UNIT ( .MILLI., .METRE. ) );
#16363=VECTOR ( 'NONE', #1811, 1000.000000000000114 ) ;
#16383=CARTESIAN_POINT ( 'NONE',  ( 2.749999999999999112, 0.000000000000000000, 0.000000000000000000 ) ) ;
#16384=DIRECTION ( 'NONE',  ( 0.000000000000000000, 0.000000000000000000, 1.000000000000000000 ) ) ;
#16424=ADVANCED_FACE ( 'NONE', ( #14181 ), #12914, .F. ) ;
#16473=CARTESIAN_POINT ( 'NONE',  ( 1.559999999999998943, 0.8660254037844428154, -1.499999999999997780 ) ) ;
#16487=LINE ( 'NONE', #4535, #8207 ) ;
#16562=VERTEX_POINT ( 'NONE', #4950 ) ;
#16565=ORIENTED_EDGE ( 'NONE', *, *, #11491, .F. ) ;
#16573=ADVANCED_FACE ( 'NONE', ( #17168 ), #13190, .F. ) ;
#16644=CIRCLE ( 'NONE', #8145, 4.750000000000000000 ) ;
#16650=DIRECTION ( 'NONE',  ( 0.000000000000000000, 0.000000000000000000, 1.000000000000000000 ) ) ;
#16673=CARTESIAN_POINT ( 'NONE',  ( 1.559999999999998943, -0.8660254037844428154, -1.499999999999997780 ) ) ;
#16685=CARTESIAN_POINT ( 'NONE',  ( 1.559999999999998943, -0.8660254037844428154, 1.500000000000001332 ) ) ;
#16740=EDGE_CURVE ( 'NONE', #8740, #374, #4999, .T. ) ;
#16741=FACE_OUTER_BOUND ( 'NONE', #5774, .T. ) ;
#16749=CARTESIAN_POINT ( 'NONE',  ( 2.950000000000001066, 0.000000000000000000, 0.000000000000000000 ) ) ;
#16758=EDGE_CURVE ( 'NONE', #1219, #9311, #8660, .T. ) ;
#16766=CARTESIAN_POINT ( 'NONE',  ( 27.75000000000000000, 2.789133085058096608E-16, -2.055000000000000160 ) ) ;
#16783=ORIENTED_EDGE ( 'NONE', *, *, #1862, .T. ) ;
#16816=CARTESIAN_POINT ( 'NONE',  ( 0.000000000000000000, 2.375000000000000000, 0.000000000000000000 ) ) ;
#16861=AXIS2_PLACEMENT_3D ( 'NONE', #7215, #9513, #8970 ) ;
#16885=AXIS2_PLACEMENT_3D ( 'NONE', #8230, #16295, #4167 ) ;
#16897=AXIS2_PLACEMENT_3D ( 'NONE', #9623, #12467, #15201 ) ;
#16934=MANIFOLD_SOLID_BREP ( 'Hex', #17419 ) ;
#16978=EDGE_CURVE ( 'NONE', #2044, #4758, #17457, .T. ) ;
#17005=ORIENTED_EDGE ( 'NONE', *, *, #7337, .T. ) ;
#17027=DIRECTION ( 'NONE',  ( 0.000000000000000000, 0.000000000000000000, 1.000000000000000000 ) ) ;
#17038=ORIENTED_EDGE ( 'NONE', *, *, #12920, .F. ) ;
#17041=PRESENTATION_STYLE_ASSIGNMENT (( #14554 ) ) ;
#17053=LINE ( 'NONE', #3513, #7225 ) ;
#17080=CARTESIAN_POINT ( 'NONE',  ( -997.5739745962155212, 0.000000000000000000, 0.000000000000000000 ) ) ;
#17092=FACE_OUTER_BOUND ( 'NONE', #1005, .T. ) ;
#17168=FACE_OUTER_BOUND ( 'NONE', #9559, .T. ) ;
#17187=DIRECTION ( 'NONE',  ( 0.000000000000000000, 0.000000000000000000, 1.000000000000000000 ) ) ;
#17206=ORIENTED_EDGE ( 'NONE', *, *, #13661, .F. ) ;
#17243=LINE ( 'NONE', #5118, #7318 ) ;
#17244=AXIS2_PLACEMENT_3D ( 'NONE', #92, #8054, #4083 ) ;
#17245=AXIS2_PLACEMENT_3D ( 'NONE', #7360, #3545, #7267 ) ;
#17301=EDGE_LOOP ( 'NONE', ( #13416, #12683 ) ) ;
#17307=SURFACE_SIDE_STYLE ('',( #6245 ) ) ;
#17360=ORIENTED_EDGE ( 'NONE', *, *, #2427, .T. ) ;
#17402=CARTESIAN_POINT ( 'NONE',  ( 0.000000000000000000, 0.8660254037844428154, -1.499999999999997780 ) ) ;
#17419=CLOSED_SHELL ( 'NONE', ( #16573, #4682, #5090, #13438, #9100, #14313, #245, #4364, #3753, #762, #13547, #4906, #15132, #16424, #8783, #5885, #2129, #14347, #11155, #15229, #12716, #6255, #10465, #16317, #336, #6268, #7844 ) ) ;
#17425=LINE ( 'NONE', #4066, #12450 ) ;
#17434=AXIS2_PLACEMENT_3D ( 'NONE', #5332, #9214, #13205 ) ;
#17457=CIRCLE ( 'NONE', #8695, 0.2000000000000000944 ) ;
#17459=DIRECTION ( 'NONE',  ( 0.000000000000000000, 0.000000000000000000, -1.000000000000000000 ) ) ;
ENDSEC;
END-ISO-10303-21;
